ISO-10303-21;
HEADER;
/* Generated by software containing ST-Developer
 * from STEP Tools, Inc. (www.steptools.com) 
 */

FILE_DESCRIPTION(
/* description */ ('Bearing housing with oil seal and end cap'),
/* implementation_level */ '2;1');

FILE_NAME(
/* name */ 'Cap Screw - M6x25.step',
/* time_stamp */ '2026-10-28T03:23:10-07:00',
/* author */ (''),
/* organization */ (''),
/* preprocessor_version */ 'ST-DEVELOPER v20.2',
/* originating_system */ 'Autodesk Translation Framework v15.17.0.0',
/* authorisation */ '');

FILE_SCHEMA (('AUTOMOTIVE_DESIGN { 1 0 10303 214 3 1 1 }'));
ENDSEC;

DATA;
#10=MECHANICAL_DESIGN_GEOMETRIC_PRESENTATION_REPRESENTATION('',(#280),#7871);
#11=ORIENTED_CLOSED_SHELL('',*,#4107,.F.);
#13=BREP_WITH_VOIDS('Body1',#4106,(#11));
#205=CONICAL_SURFACE('',#4692,0.475,0.785398163397449);
#206=CONICAL_SURFACE('',#4696,0.485,0.785398163397448);
#207=CONICAL_SURFACE('',#4700,0.31,0.463647609000806);
#208=CONICAL_SURFACE('',#4704,0.27,0.785398163397448);
#230=SHAPE_REPRESENTATION_RELATIONSHIP('SRR','None',#7978,#251);
#251=ADVANCED_BREP_SHAPE_REPRESENTATION('',(#13),#7862);
#280=STYLED_ITEM('',(#8160),#13);
#383=FACE_BOUND('',#1032,.T.);
#488=PLANE('',#4690);
#489=PLANE('',#4698);
#490=PLANE('',#4706);
#491=PLANE('',#4707);
#492=PLANE('',#4708);
#493=PLANE('',#4709);
#494=PLANE('',#4710);
#495=PLANE('',#4711);
#496=PLANE('',#4712);
#497=PLANE('',#4713);
#498=PLANE('',#4714);
#708=FACE_OUTER_BOUND('',#1027,.T.);
#709=FACE_OUTER_BOUND('',#1028,.T.);
#710=FACE_OUTER_BOUND('',#1029,.T.);
#711=FACE_OUTER_BOUND('',#1030,.T.);
#712=FACE_OUTER_BOUND('',#1031,.T.);
#713=FACE_OUTER_BOUND('',#1033,.T.);
#714=FACE_OUTER_BOUND('',#1034,.T.);
#715=FACE_OUTER_BOUND('',#1035,.T.);
#716=FACE_OUTER_BOUND('',#1036,.T.);
#717=FACE_OUTER_BOUND('',#1037,.T.);
#718=FACE_OUTER_BOUND('',#1038,.T.);
#719=FACE_OUTER_BOUND('',#1039,.T.);
#720=FACE_OUTER_BOUND('',#1040,.T.);
#721=FACE_OUTER_BOUND('',#1041,.T.);
#722=FACE_OUTER_BOUND('',#1042,.T.);
#723=FACE_OUTER_BOUND('',#1043,.T.);
#724=FACE_OUTER_BOUND('',#1044,.T.);
#1027=EDGE_LOOP('',(#3367));
#1028=EDGE_LOOP('',(#3368,#3369,#3370,#3371));
#1029=EDGE_LOOP('',(#3372,#3373,#3374,#3375));
#1030=EDGE_LOOP('',(#3376,#3377,#3378,#3379));
#1031=EDGE_LOOP('',(#3380));
#1032=EDGE_LOOP('',(#3381));
#1033=EDGE_LOOP('',(#3382,#3383,#3384,#3385));
#1034=EDGE_LOOP('',(#3386,#3387,#3388,#3389));
#1035=EDGE_LOOP('',(#3390,#3391,#3392,#3393));
#1036=EDGE_LOOP('',(#3394));
#1037=EDGE_LOOP('',(#3395,#3396,#3397,#3398));
#1038=EDGE_LOOP('',(#3399,#3400,#3401,#3402));
#1039=EDGE_LOOP('',(#3403,#3404,#3405,#3406));
#1040=EDGE_LOOP('',(#3407,#3408,#3409,#3410));
#1041=EDGE_LOOP('',(#3411,#3412,#3413,#3414));
#1042=EDGE_LOOP('',(#3415,#3416,#3417,#3418));
#1043=EDGE_LOOP('',(#3419,#3420,#3421,#3422,#3423,#3424));
#1044=EDGE_LOOP('',(#3425,#3426,#3427,#3428,#3429,#3430));
#1277=LINE('',#7256,#1539);
#1278=LINE('',#7260,#1540);
#1279=LINE('',#7264,#1541);
#1280=LINE('',#7271,#1542);
#1281=LINE('',#7275,#1543);
#1282=LINE('',#7279,#1544);
#1283=LINE('',#7284,#1545);
#1284=LINE('',#7286,#1546);
#1285=LINE('',#7288,#1547);
#1286=LINE('',#7289,#1548);
#1287=LINE('',#7292,#1549);
#1288=LINE('',#7294,#1550);
#1289=LINE('',#7295,#1551);
#1290=LINE('',#7298,#1552);
#1291=LINE('',#7300,#1553);
#1292=LINE('',#7301,#1554);
#1293=LINE('',#7304,#1555);
#1294=LINE('',#7306,#1556);
#1295=LINE('',#7307,#1557);
#1296=LINE('',#7310,#1558);
#1297=LINE('',#7312,#1559);
#1298=LINE('',#7313,#1560);
#1299=LINE('',#7315,#1561);
#1300=LINE('',#7316,#1562);
#1539=VECTOR('',#5702,0.475);
#1540=VECTOR('',#5707,0.5);
#1541=VECTOR('',#5712,0.485);
#1542=VECTOR('',#5721,0.31);
#1543=VECTOR('',#5726,0.3);
#1544=VECTOR('',#5731,0.27);
#1545=VECTOR('',#5736,1.);
#1546=VECTOR('',#5737,1.);
#1547=VECTOR('',#5738,1.);
#1548=VECTOR('',#5739,1.);
#1549=VECTOR('',#5742,1.);
#1550=VECTOR('',#5743,1.);
#1551=VECTOR('',#5744,1.);
#1552=VECTOR('',#5747,1.);
#1553=VECTOR('',#5748,1.);
#1554=VECTOR('',#5749,1.);
#1555=VECTOR('',#5752,1.);
#1556=VECTOR('',#5753,1.);
#1557=VECTOR('',#5754,1.);
#1558=VECTOR('',#5757,1.);
#1559=VECTOR('',#5758,1.);
#1560=VECTOR('',#5759,1.);
#1561=VECTOR('',#5762,1.);
#1562=VECTOR('',#5763,1.);
#1835=CIRCLE('',#4691,0.45);
#1836=CIRCLE('',#4693,0.5);
#1837=CIRCLE('',#4695,0.5);
#1838=CIRCLE('',#4697,0.47);
#1839=CIRCLE('',#4699,0.32);
#1840=CIRCLE('',#4701,0.2942);
#1841=CIRCLE('',#4703,0.2942);
#1842=CIRCLE('',#4705,0.24);
#2107=VERTEX_POINT('',#7251);
#2108=VERTEX_POINT('',#7254);
#2109=VERTEX_POINT('',#7258);
#2110=VERTEX_POINT('',#7262);
#2111=VERTEX_POINT('',#7266);
#2112=VERTEX_POINT('',#7269);
#2113=VERTEX_POINT('',#7273);
#2114=VERTEX_POINT('',#7277);
#2115=VERTEX_POINT('',#7282);
#2116=VERTEX_POINT('',#7283);
#2117=VERTEX_POINT('',#7285);
#2118=VERTEX_POINT('',#7287);
#2119=VERTEX_POINT('',#7291);
#2120=VERTEX_POINT('',#7293);
#2121=VERTEX_POINT('',#7297);
#2122=VERTEX_POINT('',#7299);
#2123=VERTEX_POINT('',#7303);
#2124=VERTEX_POINT('',#7305);
#2125=VERTEX_POINT('',#7309);
#2126=VERTEX_POINT('',#7311);
#2547=EDGE_CURVE('',#2107,#2107,#1835,.T.);
#2548=EDGE_CURVE('',#2108,#2108,#1836,.T.);
#2549=EDGE_CURVE('',#2108,#2107,#1277,.T.);
#2550=EDGE_CURVE('',#2109,#2109,#1837,.T.);
#2551=EDGE_CURVE('',#2109,#2108,#1278,.T.);
#2552=EDGE_CURVE('',#2110,#2110,#1838,.T.);
#2553=EDGE_CURVE('',#2110,#2109,#1279,.T.);
#2554=EDGE_CURVE('',#2111,#2111,#1839,.T.);
#2555=EDGE_CURVE('',#2112,#2112,#1840,.F.);
#2556=EDGE_CURVE('',#2112,#2111,#1280,.T.);
#2557=EDGE_CURVE('',#2113,#2113,#1841,.F.);
#2558=EDGE_CURVE('',#2113,#2112,#1281,.T.);
#2559=EDGE_CURVE('',#2114,#2114,#1842,.T.);
#2560=EDGE_CURVE('',#2114,#2113,#1282,.T.);
#2561=EDGE_CURVE('',#2115,#2116,#1283,.T.);
#2562=EDGE_CURVE('',#2116,#2117,#1284,.T.);
#2563=EDGE_CURVE('',#2117,#2118,#1285,.T.);
#2564=EDGE_CURVE('',#2115,#2118,#1286,.T.);
#2565=EDGE_CURVE('',#2116,#2119,#1287,.T.);
#2566=EDGE_CURVE('',#2119,#2120,#1288,.T.);
#2567=EDGE_CURVE('',#2120,#2117,#1289,.T.);
#2568=EDGE_CURVE('',#2119,#2121,#1290,.T.);
#2569=EDGE_CURVE('',#2121,#2122,#1291,.T.);
#2570=EDGE_CURVE('',#2122,#2120,#1292,.T.);
#2571=EDGE_CURVE('',#2121,#2123,#1293,.T.);
#2572=EDGE_CURVE('',#2123,#2124,#1294,.T.);
#2573=EDGE_CURVE('',#2124,#2122,#1295,.T.);
#2574=EDGE_CURVE('',#2123,#2125,#1296,.T.);
#2575=EDGE_CURVE('',#2125,#2126,#1297,.T.);
#2576=EDGE_CURVE('',#2126,#2124,#1298,.T.);
#2577=EDGE_CURVE('',#2125,#2115,#1299,.T.);
#2578=EDGE_CURVE('',#2118,#2126,#1300,.T.);
#3367=ORIENTED_EDGE('',*,*,#2547,.F.);
#3368=ORIENTED_EDGE('',*,*,#2548,.F.);
#3369=ORIENTED_EDGE('',*,*,#2549,.T.);
#3370=ORIENTED_EDGE('',*,*,#2547,.T.);
#3371=ORIENTED_EDGE('',*,*,#2549,.F.);
#3372=ORIENTED_EDGE('',*,*,#2550,.F.);
#3373=ORIENTED_EDGE('',*,*,#2551,.T.);
#3374=ORIENTED_EDGE('',*,*,#2548,.T.);
#3375=ORIENTED_EDGE('',*,*,#2551,.F.);
#3376=ORIENTED_EDGE('',*,*,#2552,.F.);
#3377=ORIENTED_EDGE('',*,*,#2553,.T.);
#3378=ORIENTED_EDGE('',*,*,#2550,.T.);
#3379=ORIENTED_EDGE('',*,*,#2553,.F.);
#3380=ORIENTED_EDGE('',*,*,#2552,.T.);
#3381=ORIENTED_EDGE('',*,*,#2554,.F.);
#3382=ORIENTED_EDGE('',*,*,#2555,.F.);
#3383=ORIENTED_EDGE('',*,*,#2556,.T.);
#3384=ORIENTED_EDGE('',*,*,#2554,.T.);
#3385=ORIENTED_EDGE('',*,*,#2556,.F.);
#3386=ORIENTED_EDGE('',*,*,#2557,.F.);
#3387=ORIENTED_EDGE('',*,*,#2558,.T.);
#3388=ORIENTED_EDGE('',*,*,#2555,.T.);
#3389=ORIENTED_EDGE('',*,*,#2558,.F.);
#3390=ORIENTED_EDGE('',*,*,#2559,.F.);
#3391=ORIENTED_EDGE('',*,*,#2560,.T.);
#3392=ORIENTED_EDGE('',*,*,#2557,.T.);
#3393=ORIENTED_EDGE('',*,*,#2560,.F.);
#3394=ORIENTED_EDGE('',*,*,#2559,.T.);
#3395=ORIENTED_EDGE('',*,*,#2561,.T.);
#3396=ORIENTED_EDGE('',*,*,#2562,.T.);
#3397=ORIENTED_EDGE('',*,*,#2563,.T.);
#3398=ORIENTED_EDGE('',*,*,#2564,.F.);
#3399=ORIENTED_EDGE('',*,*,#2565,.T.);
#3400=ORIENTED_EDGE('',*,*,#2566,.T.);
#3401=ORIENTED_EDGE('',*,*,#2567,.T.);
#3402=ORIENTED_EDGE('',*,*,#2562,.F.);
#3403=ORIENTED_EDGE('',*,*,#2568,.T.);
#3404=ORIENTED_EDGE('',*,*,#2569,.T.);
#3405=ORIENTED_EDGE('',*,*,#2570,.T.);
#3406=ORIENTED_EDGE('',*,*,#2566,.F.);
#3407=ORIENTED_EDGE('',*,*,#2571,.T.);
#3408=ORIENTED_EDGE('',*,*,#2572,.T.);
#3409=ORIENTED_EDGE('',*,*,#2573,.T.);
#3410=ORIENTED_EDGE('',*,*,#2569,.F.);
#3411=ORIENTED_EDGE('',*,*,#2574,.T.);
#3412=ORIENTED_EDGE('',*,*,#2575,.T.);
#3413=ORIENTED_EDGE('',*,*,#2576,.T.);
#3414=ORIENTED_EDGE('',*,*,#2572,.F.);
#3415=ORIENTED_EDGE('',*,*,#2577,.T.);
#3416=ORIENTED_EDGE('',*,*,#2564,.T.);
#3417=ORIENTED_EDGE('',*,*,#2578,.T.);
#3418=ORIENTED_EDGE('',*,*,#2575,.F.);
#3419=ORIENTED_EDGE('',*,*,#2577,.F.);
#3420=ORIENTED_EDGE('',*,*,#2574,.F.);
#3421=ORIENTED_EDGE('',*,*,#2571,.F.);
#3422=ORIENTED_EDGE('',*,*,#2568,.F.);
#3423=ORIENTED_EDGE('',*,*,#2565,.F.);
#3424=ORIENTED_EDGE('',*,*,#2561,.F.);
#3425=ORIENTED_EDGE('',*,*,#2578,.F.);
#3426=ORIENTED_EDGE('',*,*,#2563,.F.);
#3427=ORIENTED_EDGE('',*,*,#2567,.F.);
#3428=ORIENTED_EDGE('',*,*,#2570,.F.);
#3429=ORIENTED_EDGE('',*,*,#2573,.F.);
#3430=ORIENTED_EDGE('',*,*,#2576,.F.);
#3813=CYLINDRICAL_SURFACE('',#4694,0.5);
#3814=CYLINDRICAL_SURFACE('',#4702,0.2942);
#3990=ADVANCED_FACE('',(#708),#488,.T.);
#3991=ADVANCED_FACE('',(#709),#205,.T.);
#3992=ADVANCED_FACE('',(#710),#3813,.T.);
#3993=ADVANCED_FACE('',(#711),#206,.T.);
#3994=ADVANCED_FACE('',(#712,#383),#489,.T.);
#3995=ADVANCED_FACE('',(#713),#207,.T.);
#3996=ADVANCED_FACE('',(#714),#3814,.T.);
#3997=ADVANCED_FACE('',(#715),#208,.T.);
#3998=ADVANCED_FACE('',(#716),#490,.T.);
#3999=ADVANCED_FACE('',(#717),#491,.F.);
#4000=ADVANCED_FACE('',(#718),#492,.F.);
#4001=ADVANCED_FACE('',(#719),#493,.F.);
#4002=ADVANCED_FACE('',(#720),#494,.F.);
#4003=ADVANCED_FACE('',(#721),#495,.F.);
#4004=ADVANCED_FACE('',(#722),#496,.F.);
#4005=ADVANCED_FACE('',(#723),#497,.F.);
#4006=ADVANCED_FACE('',(#724),#498,.F.);
#4106=CLOSED_SHELL('',(#3990,#3991,#3992,#3993,#3994,#3995,#3996,#3997,
#3998));
#4107=CLOSED_SHELL('',(#3999,#4000,#4001,#4002,#4003,#4004,#4005,#4006));
#4689=AXIS2_PLACEMENT_3D('',#7249,#5692,#5693);
#4690=AXIS2_PLACEMENT_3D('',#7250,#5694,#5695);
#4691=AXIS2_PLACEMENT_3D('',#7252,#5696,#5697);
#4692=AXIS2_PLACEMENT_3D('',#7253,#5698,#5699);
#4693=AXIS2_PLACEMENT_3D('',#7255,#5700,#5701);
#4694=AXIS2_PLACEMENT_3D('',#7257,#5703,#5704);
#4695=AXIS2_PLACEMENT_3D('',#7259,#5705,#5706);
#4696=AXIS2_PLACEMENT_3D('',#7261,#5708,#5709);
#4697=AXIS2_PLACEMENT_3D('',#7263,#5710,#5711);
#4698=AXIS2_PLACEMENT_3D('',#7265,#5713,#5714);
#4699=AXIS2_PLACEMENT_3D('',#7267,#5715,#5716);
#4700=AXIS2_PLACEMENT_3D('',#7268,#5717,#5718);
#4701=AXIS2_PLACEMENT_3D('',#7270,#5719,#5720);
#4702=AXIS2_PLACEMENT_3D('',#7272,#5722,#5723);
#4703=AXIS2_PLACEMENT_3D('',#7274,#5724,#5725);
#4704=AXIS2_PLACEMENT_3D('',#7276,#5727,#5728);
#4705=AXIS2_PLACEMENT_3D('',#7278,#5729,#5730);
#4706=AXIS2_PLACEMENT_3D('',#7280,#5732,#5733);
#4707=AXIS2_PLACEMENT_3D('',#7281,#5734,#5735);
#4708=AXIS2_PLACEMENT_3D('',#7290,#5740,#5741);
#4709=AXIS2_PLACEMENT_3D('',#7296,#5745,#5746);
#4710=AXIS2_PLACEMENT_3D('',#7302,#5750,#5751);
#4711=AXIS2_PLACEMENT_3D('',#7308,#5755,#5756);
#4712=AXIS2_PLACEMENT_3D('',#7314,#5760,#5761);
#4713=AXIS2_PLACEMENT_3D('',#7317,#5764,#5765);
#4714=AXIS2_PLACEMENT_3D('',#7318,#5766,#5767);
#5692=DIRECTION('axis',(0.,0.,1.));
#5693=DIRECTION('refdir',(1.,0.,0.));
#5694=DIRECTION('center_axis',(0.,1.,0.));
#5695=DIRECTION('ref_axis',(0.,0.,1.));
#5696=DIRECTION('center_axis',(0.,-1.,0.));
#5697=DIRECTION('ref_axis',(1.,0.,0.));
#5698=DIRECTION('center_axis',(0.,-1.,0.));
#5699=DIRECTION('ref_axis',(1.,0.,0.));
#5700=DIRECTION('center_axis',(0.,-1.,0.));
#5701=DIRECTION('ref_axis',(1.,0.,0.));
#5702=DIRECTION('',(0.707106781186548,0.707106781186547,8.65956056235494E-17));
#5703=DIRECTION('center_axis',(0.,-1.,0.));
#5704=DIRECTION('ref_axis',(1.,0.,0.));
#5705=DIRECTION('center_axis',(0.,-1.,0.));
#5706=DIRECTION('ref_axis',(1.,0.,0.));
#5707=DIRECTION('',(0.,1.,0.));
#5708=DIRECTION('center_axis',(0.,1.,0.));
#5709=DIRECTION('ref_axis',(1.,0.,0.));
#5710=DIRECTION('center_axis',(0.,-1.,0.));
#5711=DIRECTION('ref_axis',(1.,0.,0.));
#5712=DIRECTION('',(-0.707106781186547,0.707106781186548,-8.65956056235493E-17));
#5713=DIRECTION('center_axis',(0.,-1.,0.));
#5714=DIRECTION('ref_axis',(0.,0.,-1.));
#5715=DIRECTION('center_axis',(0.,-1.,0.));
#5716=DIRECTION('ref_axis',(1.,0.,0.));
#5717=DIRECTION('center_axis',(0.,1.,0.));
#5718=DIRECTION('ref_axis',(1.,0.,0.));
#5719=DIRECTION('center_axis',(0.,1.,0.));
#5720=DIRECTION('ref_axis',(1.,0.,0.));
#5721=DIRECTION('',(-0.447213595499958,0.894427190999916,-5.47678698264203E-17));
#5722=DIRECTION('center_axis',(0.,-1.,0.));
#5723=DIRECTION('ref_axis',(1.,0.,0.));
#5724=DIRECTION('center_axis',(0.,1.,0.));
#5725=DIRECTION('ref_axis',(1.,0.,0.));
#5726=DIRECTION('',(0.,1.,0.));
#5727=DIRECTION('center_axis',(0.,1.,0.));
#5728=DIRECTION('ref_axis',(1.,0.,0.));
#5729=DIRECTION('center_axis',(0.,-1.,0.));
#5730=DIRECTION('ref_axis',(1.,0.,0.));
#5731=DIRECTION('',(-0.707106781186547,0.707106781186548,-8.65956056235493E-17));
#5732=DIRECTION('center_axis',(0.,-1.,0.));
#5733=DIRECTION('ref_axis',(0.,0.,-1.));
#5734=DIRECTION('center_axis',(0.866025403784439,0.,-0.5));
#5735=DIRECTION('ref_axis',(0.5,0.,0.866025403784439));
#5736=DIRECTION('',(-0.5,0.,-0.866025403784439));
#5737=DIRECTION('',(0.,-1.,0.));
#5738=DIRECTION('',(0.5,0.,0.866025403784439));
#5739=DIRECTION('',(0.,-1.,0.));
#5740=DIRECTION('center_axis',(1.92296268638356E-16,0.,-1.));
#5741=DIRECTION('ref_axis',(1.,0.,1.92296268638356E-16));
#5742=DIRECTION('',(-1.,0.,-1.92296268638356E-16));
#5743=DIRECTION('',(0.,-1.,0.));
#5744=DIRECTION('',(1.,0.,1.92296268638356E-16));
#5745=DIRECTION('center_axis',(-0.866025403784439,0.,-0.5));
#5746=DIRECTION('ref_axis',(0.5,0.,-0.866025403784439));
#5747=DIRECTION('',(-0.5,0.,0.866025403784438));
#5748=DIRECTION('',(0.,-1.,0.));
#5749=DIRECTION('',(0.5,0.,-0.866025403784438));
#5750=DIRECTION('center_axis',(-0.866025403784439,0.,0.5));
#5751=DIRECTION('ref_axis',(-0.5,0.,-0.866025403784439));
#5752=DIRECTION('',(0.5,0.,0.866025403784439));
#5753=DIRECTION('',(0.,-1.,0.));
#5754=DIRECTION('',(-0.5,0.,-0.866025403784439));
#5755=DIRECTION('center_axis',(-1.92296268638356E-16,0.,1.));
#5756=DIRECTION('ref_axis',(-1.,0.,-1.92296268638356E-16));
#5757=DIRECTION('',(1.,0.,1.92296268638356E-16));
#5758=DIRECTION('',(0.,-1.,0.));
#5759=DIRECTION('',(-1.,0.,-1.92296268638356E-16));
#5760=DIRECTION('center_axis',(0.866025403784439,0.,0.5));
#5761=DIRECTION('ref_axis',(-0.5,0.,0.866025403784439));
#5762=DIRECTION('',(0.5,0.,-0.866025403784439));
#5763=DIRECTION('',(-0.5,0.,0.866025403784439));
#5764=DIRECTION('center_axis',(0.,1.,0.));
#5765=DIRECTION('ref_axis',(1.,0.,0.));
#5766=DIRECTION('center_axis',(0.,-1.,0.));
#5767=DIRECTION('ref_axis',(0.,0.,-1.));
#7249=CARTESIAN_POINT('',(0.,0.,0.));
#7250=CARTESIAN_POINT('Origin',(0.45,0.6,0.));
#7251=CARTESIAN_POINT('',(-0.45,0.6,-5.51091059616309E-17));
#7252=CARTESIAN_POINT('Origin',(0.,0.6,0.));
#7253=CARTESIAN_POINT('Origin',(0.,0.575,0.));
#7254=CARTESIAN_POINT('',(-0.5,0.55,-6.12323399573677E-17));
#7255=CARTESIAN_POINT('Origin',(0.,0.55,0.));
#7256=CARTESIAN_POINT('',(-0.475,0.575,-5.81707229594993E-17));
#7257=CARTESIAN_POINT('Origin',(0.,0.29,0.));
#7258=CARTESIAN_POINT('',(-0.5,0.0299999999999998,-6.12323399573677E-17));
#7259=CARTESIAN_POINT('Origin',(0.,0.0299999999999998,0.));
#7260=CARTESIAN_POINT('',(-0.5,0.29,-6.12323399573677E-17));
#7261=CARTESIAN_POINT('Origin',(0.,0.0150000000000001,0.));
#7262=CARTESIAN_POINT('',(-0.47,7.11236625150491E-17,-5.75583995599256E-17));
#7263=CARTESIAN_POINT('Origin',(0.,0.,0.));
#7264=CARTESIAN_POINT('',(-0.485,0.0150000000000001,-5.93953697586466E-17));
#7265=CARTESIAN_POINT('Origin',(0.32,0.,0.));
#7266=CARTESIAN_POINT('',(-0.32,-6.93889390390723E-18,-3.91886975727153E-17));
#7267=CARTESIAN_POINT('Origin',(0.,0.,0.));
#7268=CARTESIAN_POINT('Origin',(0.,-0.02,0.));
#7269=CARTESIAN_POINT('',(-0.2942,-0.0515999999999999,3.60291088309151E-17));
#7270=CARTESIAN_POINT('Origin',(0.,-0.0515999999999999,0.));
#7271=CARTESIAN_POINT('',(-0.31,-0.02,-3.7964050773568E-17));
#7272=CARTESIAN_POINT('Origin',(0.,-1.24,0.));
#7273=CARTESIAN_POINT('',(-0.2942,-2.4458,3.60291088309151E-17));
#7274=CARTESIAN_POINT('Origin',(0.,-2.4458,0.));
#7275=CARTESIAN_POINT('',(-0.2942,-1.24,-3.60291088309151E-17));
#7276=CARTESIAN_POINT('Origin',(0.,-2.47,0.));
#7277=CARTESIAN_POINT('',(-0.24,-2.5,-2.93915231795365E-17));
#7278=CARTESIAN_POINT('Origin',(0.,-2.5,0.));
#7279=CARTESIAN_POINT('',(-0.27,-2.47,-3.30654635769785E-17));
#7280=CARTESIAN_POINT('Origin',(0.,-2.5,0.));
#7281=CARTESIAN_POINT('Origin',(0.144337567297406,-0.6,-0.25));
#7282=CARTESIAN_POINT('',(0.288675134594813,-0.6,0.));
#7283=CARTESIAN_POINT('',(0.144337567297406,-0.6,-0.25));
#7284=CARTESIAN_POINT('',(0.288675134594813,-0.6,0.));
#7285=CARTESIAN_POINT('',(0.144337567297406,-0.96,-0.25));
#7286=CARTESIAN_POINT('',(0.144337567297406,-0.6,-0.25));
#7287=CARTESIAN_POINT('',(0.288675134594813,-0.96,0.));
#7288=CARTESIAN_POINT('',(0.288675134594813,-0.96,0.));
#7289=CARTESIAN_POINT('',(0.288675134594813,-0.6,0.));
#7290=CARTESIAN_POINT('Origin',(-0.144337567297406,-0.6,-0.25));
#7291=CARTESIAN_POINT('',(-0.144337567297406,-0.6,-0.25));
#7292=CARTESIAN_POINT('',(0.144337567297406,-0.6,-0.25));
#7293=CARTESIAN_POINT('',(-0.144337567297406,-0.96,-0.25));
#7294=CARTESIAN_POINT('',(-0.144337567297406,-0.6,-0.25));
#7295=CARTESIAN_POINT('',(0.144337567297406,-0.96,-0.25));
#7296=CARTESIAN_POINT('Origin',(-0.288675134594813,-0.6,-8.32667268468867E-17));
#7297=CARTESIAN_POINT('',(-0.288675134594813,-0.6,-3.53525079574969E-17));
#7298=CARTESIAN_POINT('',(-0.144337567297406,-0.6,-0.25));
#7299=CARTESIAN_POINT('',(-0.288675134594813,-0.96,-5.55111512312578E-17));
#7300=CARTESIAN_POINT('',(-0.288675134594813,-0.6,-3.53525079574969E-17));
#7301=CARTESIAN_POINT('',(-0.144337567297406,-0.96,-0.25));
#7302=CARTESIAN_POINT('Origin',(-0.144337567297407,-0.6,0.25));
#7303=CARTESIAN_POINT('',(-0.144337567297407,-0.6,0.25));
#7304=CARTESIAN_POINT('',(-0.288675134594813,-0.6,-3.53525079574969E-17));
#7305=CARTESIAN_POINT('',(-0.144337567297407,-0.96,0.25));
#7306=CARTESIAN_POINT('',(-0.144337567297407,-0.6,0.25));
#7307=CARTESIAN_POINT('',(-0.288675134594813,-0.96,-3.53525079574969E-17));
#7308=CARTESIAN_POINT('Origin',(0.144337567297406,-0.6,0.25));
#7309=CARTESIAN_POINT('',(0.144337567297406,-0.6,0.25));
#7310=CARTESIAN_POINT('',(-0.144337567297407,-0.6,0.25));
#7311=CARTESIAN_POINT('',(0.144337567297406,-0.96,0.25));
#7312=CARTESIAN_POINT('',(0.144337567297406,-0.6,0.25));
#7313=CARTESIAN_POINT('',(-0.144337567297407,-0.96,0.25));
#7314=CARTESIAN_POINT('Origin',(0.288675134594813,-0.6,0.));
#7315=CARTESIAN_POINT('',(0.144337567297406,-0.6,0.25));
#7316=CARTESIAN_POINT('',(0.144337567297406,-0.96,0.25));
#7317=CARTESIAN_POINT('Origin',(0.,-0.6,0.));
#7318=CARTESIAN_POINT('Origin',(0.,-0.96,0.));
#7836=UNCERTAINTY_MEASURE_WITH_UNIT(LENGTH_MEASURE(0.001),#7872,
'DISTANCE_ACCURACY_VALUE',
'Maximum model space distance between geometric entities at asserted c
onnectivities');
#7845=UNCERTAINTY_MEASURE_WITH_UNIT(LENGTH_MEASURE(0.001),#7872,
'DISTANCE_ACCURACY_VALUE',
'Maximum model space distance between geometric entities at asserted c
onnectivities');
#7862=(
GEOMETRIC_REPRESENTATION_CONTEXT(3)
GLOBAL_UNCERTAINTY_ASSIGNED_CONTEXT((#7836))
GLOBAL_UNIT_ASSIGNED_CONTEXT((#7872,#7874,#7875))
REPRESENTATION_CONTEXT('','3D')
);
#7871=(
GEOMETRIC_REPRESENTATION_CONTEXT(3)
GLOBAL_UNCERTAINTY_ASSIGNED_CONTEXT((#7845))
GLOBAL_UNIT_ASSIGNED_CONTEXT((#7872,#7874,#7875))
REPRESENTATION_CONTEXT('','3D')
);
#7872=(
LENGTH_UNIT()
NAMED_UNIT(*)
SI_UNIT(.CENTI.,.METRE.)
);
#7874=(
NAMED_UNIT(*)
PLANE_ANGLE_UNIT()
SI_UNIT($,.RADIAN.)
);
#7875=(
NAMED_UNIT(*)
SI_UNIT($,.STERADIAN.)
SOLID_ANGLE_UNIT()
);
#7892=SHAPE_DEFINITION_REPRESENTATION(#7922,#7978);
#7922=PRODUCT_DEFINITION_SHAPE('',$,#8004);
#7978=SHAPE_REPRESENTATION('',(#4689),#7862);
#7987=PRODUCT_DEFINITION_CONTEXT('part definition',#8064,'design');
#8004=PRODUCT_DEFINITION('Cap Screw - M6x25','Cap Screw - M6x25',#8029,
#7987);
#8029=PRODUCT_DEFINITION_FORMATION('',$,#8082);
#8064=APPLICATION_CONTEXT(
'Core Data for Automotive Mechanical Design Process');
#8065=PRODUCT_CONTEXT('part definition',#8064,'mechanical');
#8082=PRODUCT('Cap Screw - M6x25','Cap Screw - M6x25',
'Cap Screw - M6x25',(#8065));
#8154=COLOUR_RGB('Black',0.12,0.14,0.17);
#8155=FILL_AREA_STYLE_COLOUR('',#8154);
#8156=FILL_AREA_STYLE('',(#8155));
#8157=SURFACE_STYLE_FILL_AREA(#8156);
#8158=SURFACE_SIDE_STYLE('',(#8157));
#8159=SURFACE_STYLE_USAGE(.BOTH.,#8158);
#8160=PRESENTATION_STYLE_ASSIGNMENT((#8159));
ENDSEC;
END-ISO-10303-21;
